ISO-10303-21;
HEADER;
/* Generated by software containing ST-Developer
 * from STEP Tools, Inc. (www.steptools.com) 
 */

FILE_DESCRIPTION(
/* description */ ('Turntable on roller ring'),
/* implementation_level */ '2;1');

FILE_NAME(
/* name */ 'Inner race spacer (6).step',
/* time_stamp */ '2026-10-28T03:23:59-07:00',
/* author */ (''),
/* organization */ (''),
/* preprocessor_version */ 'ST-DEVELOPER v20.2',
/* originating_system */ 'Autodesk Translation Framework v15.17.0.0',
/* authorisation */ '');

FILE_SCHEMA (('AUTOMOTIVE_DESIGN { 1 0 10303 214 3 1 1 }'));
ENDSEC;

DATA;
#10=MECHANICAL_DESIGN_GEOMETRIC_PRESENTATION_REPRESENTATION('',(#659),#16281);
#540=SHAPE_REPRESENTATION_RELATIONSHIP('SRR','None',#16560,#595);
#595=ADVANCED_BREP_SHAPE_REPRESENTATION('',(#729),#16254);
#659=STYLED_ITEM('',(#16932),#729);
#729=MANIFOLD_SOLID_BREP('Body1',#8402);
#949=FACE_BOUND('',#2312,.T.);
#950=FACE_BOUND('',#2314,.T.);
#1181=PLANE('',#9820);
#1182=PLANE('',#9821);
#1612=FACE_OUTER_BOUND('',#2309,.T.);
#1613=FACE_OUTER_BOUND('',#2310,.T.);
#1614=FACE_OUTER_BOUND('',#2311,.T.);
#1615=FACE_OUTER_BOUND('',#2313,.T.);
#2309=EDGE_LOOP('',(#7157,#7158,#7159,#7160));
#2310=EDGE_LOOP('',(#7161,#7162,#7163,#7164));
#2311=EDGE_LOOP('',(#7165));
#2312=EDGE_LOOP('',(#7166));
#2313=EDGE_LOOP('',(#7167));
#2314=EDGE_LOOP('',(#7168));
#2884=LINE('',#15136,#3367);
#2885=LINE('',#15142,#3368);
#3367=VECTOR('',#12143,0.505);
#3368=VECTOR('',#12150,0.7);
#3803=CIRCLE('',#9815,0.505);
#3804=CIRCLE('',#9816,0.505);
#3805=CIRCLE('',#9818,0.7);
#3806=CIRCLE('',#9819,0.7);
#4455=VERTEX_POINT('',#15133);
#4456=VERTEX_POINT('',#15135);
#4457=VERTEX_POINT('',#15139);
#4458=VERTEX_POINT('',#15141);
#5389=EDGE_CURVE('',#4455,#4455,#3803,.T.);
#5390=EDGE_CURVE('',#4455,#4456,#2884,.T.);
#5391=EDGE_CURVE('',#4456,#4456,#3804,.T.);
#5392=EDGE_CURVE('',#4457,#4457,#3805,.T.);
#5393=EDGE_CURVE('',#4457,#4458,#2885,.T.);
#5394=EDGE_CURVE('',#4458,#4458,#3806,.T.);
#7157=ORIENTED_EDGE('',*,*,#5389,.F.);
#7158=ORIENTED_EDGE('',*,*,#5390,.T.);
#7159=ORIENTED_EDGE('',*,*,#5391,.T.);
#7160=ORIENTED_EDGE('',*,*,#5390,.F.);
#7161=ORIENTED_EDGE('',*,*,#5392,.F.);
#7162=ORIENTED_EDGE('',*,*,#5393,.T.);
#7163=ORIENTED_EDGE('',*,*,#5394,.T.);
#7164=ORIENTED_EDGE('',*,*,#5393,.F.);
#7165=ORIENTED_EDGE('',*,*,#5392,.T.);
#7166=ORIENTED_EDGE('',*,*,#5389,.T.);
#7167=ORIENTED_EDGE('',*,*,#5394,.F.);
#7168=ORIENTED_EDGE('',*,*,#5391,.F.);
#7807=CYLINDRICAL_SURFACE('',#9814,0.505);
#7808=CYLINDRICAL_SURFACE('',#9817,0.7);
#8215=ADVANCED_FACE('',(#1612),#7807,.F.);
#8216=ADVANCED_FACE('',(#1613),#7808,.T.);
#8217=ADVANCED_FACE('',(#1614,#949),#1181,.T.);
#8218=ADVANCED_FACE('',(#1615,#950),#1182,.F.);
#8402=CLOSED_SHELL('',(#8215,#8216,#8217,#8218));
#9813=AXIS2_PLACEMENT_3D('',#15131,#12137,#12138);
#9814=AXIS2_PLACEMENT_3D('',#15132,#12139,#12140);
#9815=AXIS2_PLACEMENT_3D('',#15134,#12141,#12142);
#9816=AXIS2_PLACEMENT_3D('',#15137,#12144,#12145);
#9817=AXIS2_PLACEMENT_3D('',#15138,#12146,#12147);
#9818=AXIS2_PLACEMENT_3D('',#15140,#12148,#12149);
#9819=AXIS2_PLACEMENT_3D('',#15143,#12151,#12152);
#9820=AXIS2_PLACEMENT_3D('',#15144,#12153,#12154);
#9821=AXIS2_PLACEMENT_3D('',#15145,#12155,#12156);
#12137=DIRECTION('axis',(0.,0.,1.));
#12138=DIRECTION('refdir',(1.,0.,0.));
#12139=DIRECTION('center_axis',(0.,1.,0.));
#12140=DIRECTION('ref_axis',(1.,0.,0.));
#12141=DIRECTION('center_axis',(0.,-1.,0.));
#12142=DIRECTION('ref_axis',(1.,0.,0.));
#12143=DIRECTION('',(0.,-1.,0.));
#12144=DIRECTION('center_axis',(0.,-1.,0.));
#12145=DIRECTION('ref_axis',(1.,0.,0.));
#12146=DIRECTION('center_axis',(0.,1.,0.));
#12147=DIRECTION('ref_axis',(1.,0.,0.));
#12148=DIRECTION('center_axis',(0.,1.,0.));
#12149=DIRECTION('ref_axis',(1.,0.,0.));
#12150=DIRECTION('',(0.,-1.,0.));
#12151=DIRECTION('center_axis',(0.,1.,0.));
#12152=DIRECTION('ref_axis',(1.,0.,0.));
#12153=DIRECTION('center_axis',(0.,1.,0.));
#12154=DIRECTION('ref_axis',(1.,0.,0.));
#12155=DIRECTION('center_axis',(0.,1.,0.));
#12156=DIRECTION('ref_axis',(1.,0.,0.));
#15131=CARTESIAN_POINT('',(0.,0.,0.));
#15132=CARTESIAN_POINT('Origin',(0.,14.1,3.5));
#15133=CARTESIAN_POINT('',(-0.505,14.55,3.5));
#15134=CARTESIAN_POINT('Origin',(0.,14.55,3.5));
#15135=CARTESIAN_POINT('',(-0.505,14.1,3.5));
#15136=CARTESIAN_POINT('',(-0.505,14.1,3.5));
#15137=CARTESIAN_POINT('Origin',(0.,14.1,3.5));
#15138=CARTESIAN_POINT('Origin',(0.,14.1,3.5));
#15139=CARTESIAN_POINT('',(-0.7,14.55,3.5));
#15140=CARTESIAN_POINT('Origin',(0.,14.55,3.5));
#15141=CARTESIAN_POINT('',(-0.7,14.1,3.5));
#15142=CARTESIAN_POINT('',(-0.7,14.1,3.5));
#15143=CARTESIAN_POINT('Origin',(0.,14.1,3.5));
#15144=CARTESIAN_POINT('Origin',(0.,14.55,3.5));
#15145=CARTESIAN_POINT('Origin',(0.,14.1,3.5));
#16185=UNCERTAINTY_MEASURE_WITH_UNIT(LENGTH_MEASURE(0.001),#16282,
'DISTANCE_ACCURACY_VALUE',
'Maximum model space distance between geometric entities at asserted c
onnectivities');
#16212=UNCERTAINTY_MEASURE_WITH_UNIT(LENGTH_MEASURE(0.001),#16282,
'DISTANCE_ACCURACY_VALUE',
'Maximum model space distance between geometric entities at asserted c
onnectivities');
#16254=(
GEOMETRIC_REPRESENTATION_CONTEXT(3)
GLOBAL_UNCERTAINTY_ASSIGNED_CONTEXT((#16185))
GLOBAL_UNIT_ASSIGNED_CONTEXT((#16282,#16284,#16285))
REPRESENTATION_CONTEXT('','3D')
);
#16281=(
GEOMETRIC_REPRESENTATION_CONTEXT(3)
GLOBAL_UNCERTAINTY_ASSIGNED_CONTEXT((#16212))
GLOBAL_UNIT_ASSIGNED_CONTEXT((#16282,#16284,#16285))
REPRESENTATION_CONTEXT('','3D')
);
#16282=(
LENGTH_UNIT()
NAMED_UNIT(*)
SI_UNIT(.CENTI.,.METRE.)
);
#16284=(
NAMED_UNIT(*)
PLANE_ANGLE_UNIT()
SI_UNIT($,.RADIAN.)
);
#16285=(
NAMED_UNIT(*)
SI_UNIT($,.STERADIAN.)
SOLID_ANGLE_UNIT()
);
#16327=SHAPE_DEFINITION_REPRESENTATION(#16421,#16560);
#16421=PRODUCT_DEFINITION_SHAPE('',$,#16629);
#16560=SHAPE_REPRESENTATION('',(#9813),#16254);
#16587=PRODUCT_DEFINITION_CONTEXT('part definition',#16793,'design');
#16629=PRODUCT_DEFINITION('Inner race spacer (6)','Inner race spacer (6)',
#16697,#16587);
#16697=PRODUCT_DEFINITION_FORMATION('',$,#16836);
#16793=APPLICATION_CONTEXT(
'Core Data for Automotive Mechanical Design Process');
#16794=PRODUCT_CONTEXT('part definition',#16793,'mechanical');
#16836=PRODUCT('Inner race spacer (6)','Inner race spacer (6)',
'Inner race spacer (6)',(#16794));
#16926=COLOUR_RGB('Grey',0.48,0.52,0.57);
#16927=FILL_AREA_STYLE_COLOUR('',#16926);
#16928=FILL_AREA_STYLE('',(#16927));
#16929=SURFACE_STYLE_FILL_AREA(#16928);
#16930=SURFACE_SIDE_STYLE('',(#16929));
#16931=SURFACE_STYLE_USAGE(.BOTH.,#16930);
#16932=PRESENTATION_STYLE_ASSIGNMENT((#16931));
ENDSEC;
END-ISO-10303-21;
